ISO-10303-21;
HEADER;
FILE_DESCRIPTION (('STEP AP214'),
    '1' );
FILE_NAME ('socket button head screw_iso_ISO 7380 - M3 x 6 - 6N.step',
    '2026-10-22T12:35:56',
    ( '' ),
    ( '' ),
    'SwSTEP 2.0',
    'SolidWorks 2026',
    '' );
FILE_SCHEMA (( 'AUTOMOTIVE_DESIGN' ));
ENDSEC;

DATA;
#8=PRODUCT_DEFINITION_SHAPE ( 'NONE', 'NONE',  #499 ) ;
#9=PLANE ( 'NONE',  #1983 ) ;
#24=ADVANCED_FACE ( 'NONE', ( #42 ), #1841, .F. ) ;
#25=DIRECTION ( 'NONE',  ( 0.000000000000000000, 0.000000000000000000, 1.000000000000000000 ) ) ;
#26=CARTESIAN_POINT ( 'NONE',  ( 1.040000000000000036, 0.5773502691896263972, 1.000000000000000000 ) ) ;
#27=MANIFOLD_SOLID_BREP ( 'Hex', #3139 ) ;
#29=ADVANCED_FACE ( 'NONE', ( #74 ), #315, .T. ) ;
#35=LINE ( 'NONE', #521, #2562 ) ;
#42=FACE_OUTER_BOUND ( 'NONE', #272, .T. ) ;
#43=ORIENTED_EDGE ( 'NONE', *, *, #1446, .F. ) ;
#45=CIRCLE ( 'NONE', #370, 1.000000000000000000 ) ;
#49=ORIENTED_EDGE ( 'NONE', *, *, #85, .F. ) ;
#50=SPHERICAL_SURFACE ( 'NONE', #2615, 3.351416843938785028 ) ;
#52=ORIENTED_EDGE ( 'NONE', *, *, #1044, .F. ) ;
#59=DIRECTION ( 'NONE',  ( -1.000000000000000000, -0.000000000000000000, -0.000000000000000000 ) ) ;
#74=FACE_OUTER_BOUND ( 'NONE', #1738, .T. ) ;
#75=ORIENTED_EDGE ( 'NONE', *, *, #1227, .F. ) ;
#79=VERTEX_POINT ( 'NONE', #2378 ) ;
#82=CARTESIAN_POINT ( 'NONE',  ( 0.000000000000000000, -1.154700538379251684, -1.199226976249124676E-17 ) ) ;
#85=EDGE_CURVE ( 'NONE', #373, #1694, #545, .T. ) ;
#88=EDGE_LOOP ( 'NONE', ( #2505, #344, #500, #2889 ) ) ;
#93=CARTESIAN_POINT ( 'NONE',  ( 1.040000000000000036, 0.000000000000000000, 0.000000000000000000 ) ) ;
#100=ADVANCED_FACE ( 'NONE', ( #2884 ), #1598, .T. ) ;
#103=PLANE ( 'NONE',  #1529 ) ;
#110=AXIS2_PLACEMENT_3D ( 'NONE', #2236, #2915, #685 ) ;
#111=CARTESIAN_POINT ( 'NONE',  ( 0.000000000000000000, -0.5773502691896253980, -1.000000000000000000 ) ) ;
#117=ORIENTED_EDGE ( 'NONE', *, *, #85, .T. ) ;
#123=ADVANCED_FACE ( 'NONE', ( #1123 ), #857, .F. ) ;
#124=DIRECTION ( 'NONE',  ( 0.000000000000000000, 0.000000000000000000, 1.000000000000000000 ) ) ;
#131=ORIENTED_EDGE ( 'NONE', *, *, #566, .F. ) ;
#138=DIRECTION ( 'NONE',  ( 0.000000000000000000, 0.000000000000000000, 1.000000000000000000 ) ) ;
#141=DIRECTION ( 'NONE',  ( 0.000000000000000000, 0.5000000000000000000, -0.8660254037844385966 ) ) ;
#144=ORIENTED_EDGE ( 'NONE', *, *, #1772, .F. ) ;
#145=CARTESIAN_POINT ( 'NONE',  ( 1.750000000000000000, 0.000000000000000000, 1.599999999999999645 ) ) ;
#146=ORIENTED_EDGE ( 'NONE', *, *, #761, .F. ) ;
#151=EDGE_CURVE ( 'NONE', #2355, #2373, #2846, .T. ) ;
#152=ORIENTED_EDGE ( 'NONE', *, *, #660, .F. ) ;
#154=CARTESIAN_POINT ( 'NONE',  ( 7.650000000000000355, 0.000000000000000000, 1.219500000000000028 ) ) ;
#155=CIRCLE ( 'NONE', #2344, 1.219500000000000028 ) ;
#157=CIRCLE ( 'NONE', #321, 1.000000000000000000 ) ;
#160=DIRECTION ( 'NONE',  ( 0.000000000000000000, 0.000000000000000000, 1.000000000000000000 ) ) ;
#162=ORIENTED_EDGE ( 'NONE', *, *, #2964, .F. ) ;
#169=VERTEX_POINT ( 'NONE', #2407 ) ;
#171=FACE_OUTER_BOUND ( 'NONE', #213, .T. ) ;
#175=DIRECTION ( 'NONE',  ( 0.000000000000000000, -0.8660254037844387076, 0.5000000000000001110 ) ) ;
#176=ADVANCED_FACE ( 'NONE', ( #427 ), #103, .T. ) ;
#184=EDGE_CURVE ( 'NONE', #3095, #2373, #706, .T. ) ;
#187=CARTESIAN_POINT ( 'NONE',  ( -998.3826497308103853, 0.000000000000000000, 0.000000000000000000 ) ) ;
#199=ORIENTED_EDGE ( 'NONE', *, *, #759, .F. ) ;
#200=DIRECTION ( 'NONE',  ( 0.000000000000000000, 0.5000000000000003331, 0.8660254037844383745 ) ) ;
#201=AXIS2_PLACEMENT_3D ( 'NONE', #1093, #2094, #1700 ) ;
#202=DIRECTION ( 'NONE',  ( 1.000000000000000000, 0.000000000000000000, 0.000000000000000000 ) ) ;
#203=DIRECTION ( 'NONE',  ( 0.000000000000000000, 1.224646799147353207E-16, -1.000000000000000000 ) ) ;
#213=EDGE_LOOP ( 'NONE', ( #2871, #2225, #753, #2533, #2320 ) ) ;
#214=DIRECTION ( 'NONE',  ( -1.000000000000000000, -0.000000000000000000, -0.000000000000000000 ) ) ;
#215=AXIS2_PLACEMENT_3D ( 'NONE', #2706, #2727, #977 ) ;
#220=EDGE_CURVE ( 'NONE', #2839, #2850, #1722, .T. ) ;
#221=CYLINDRICAL_SURFACE ( 'NONE', #842, 2.849999999999999645 ) ;
#229=AXIS2_PLACEMENT_3D ( 'NONE', #2936, #1181, #25 ) ;
#239=CARTESIAN_POINT ( 'NONE',  ( 7.650000000000000355, 0.000000000000000000, 0.000000000000000000 ) ) ;
#244=DIRECTION ( 'NONE',  ( 0.000000000000000000, 0.000000000000000000, 1.000000000000000000 ) ) ;
#249=DIRECTION ( 'NONE',  ( 0.000000000000000000, 0.000000000000000000, 1.000000000000000000 ) ) ;
#250=DIRECTION ( 'NONE',  ( -1.000000000000000000, -0.000000000000000000, -0.000000000000000000 ) ) ;
#257=EDGE_CURVE ( 'NONE', #3213, #626, #2525, .T. ) ;
#261=LINE ( 'NONE', #26, #3174 ) ;
#265=DIRECTION ( 'NONE',  ( 0.000000000000000000, 0.000000000000000000, 1.000000000000000000 ) ) ;
#270=EDGE_CURVE ( 'NONE', #2818, #2355, #2189, .T. ) ;
#272=EDGE_LOOP ( 'NONE', ( #2012, #2992, #144 ) ) ;
#281=DIRECTION ( 'NONE',  ( 1.000000000000000000, 0.000000000000000000, -0.000000000000000000 ) ) ;
#283=ORIENTED_EDGE ( 'NONE', *, *, #1044, .T. ) ;
#291=CARTESIAN_POINT ( 'NONE',  ( 1.040000000000000036, 0.8660254037844390407, 0.5000000000000002220 ) ) ;
#292=FILL_AREA_STYLE_COLOUR ( '', #2366 ) ;
#305=ORIENTED_EDGE ( 'NONE', *, *, #748, .T. ) ;
#315=SPHERICAL_SURFACE ( 'NONE', #1477, 3.351416843938785028 ) ;
#316=ORIENTED_EDGE ( 'NONE', *, *, #1433, .F. ) ;
#321=AXIS2_PLACEMENT_3D ( 'NONE', #2470, #438, #717 ) ;
#328=CARTESIAN_POINT ( 'NONE',  ( 1.649999999999999911, 1.959434878635764737E-16, -1.599999999999999645 ) ) ;
#334=CARTESIAN_POINT ( 'NONE',  ( 1.040000000000000036, 0.5773502691896263972, 1.000000000000000000 ) ) ;
#336=ORIENTED_EDGE ( 'NONE', *, *, #257, .F. ) ;
#337=EDGE_CURVE ( 'NONE', #658, #1756, #1956, .T. ) ;
#342=DIRECTION ( 'NONE',  ( -1.000000000000000000, -0.000000000000000000, -0.000000000000000000 ) ) ;
#343=PRESENTATION_STYLE_ASSIGNMENT (( #1574 ) ) ;
#344=ORIENTED_EDGE ( 'NONE', *, *, #354, .T. ) ;
#348=( LENGTH_UNIT ( ) NAMED_UNIT ( * ) SI_UNIT ( .MILLI., .METRE. ) );
#350=CARTESIAN_POINT ( 'NONE',  ( 1.040000000000000036, -0.5773502691896253980, -1.000000000000000000 ) ) ;
#351=DIRECTION ( 'NONE',  ( -0.000000000000000000, -0.5000000000000003331, -0.8660254037844383745 ) ) ;
#352=EDGE_LOOP ( 'NONE', ( #52, #897, #2546 ) ) ;
#354=EDGE_CURVE ( 'NONE', #2839, #488, #2984, .T. ) ;
#369=DIRECTION ( 'NONE',  ( -0.000000000000000000, 1.000000000000000000, 1.224646799147353207E-16 ) ) ;
#370=AXIS2_PLACEMENT_3D ( 'NONE', #3118, #1653, #1136 ) ;
#373=VERTEX_POINT ( 'NONE', #2492 ) ;
#377=AXIS2_PLACEMENT_3D ( 'NONE', #2479, #250, #1805 ) ;
#384=ORIENTED_EDGE ( 'NONE', *, *, #1446, .T. ) ;
#385=CARTESIAN_POINT ( 'NONE',  ( 1.040000000000000036, 0.000000000000000000, 0.000000000000000000 ) ) ;
#391=VERTEX_POINT ( 'NONE', #2955 ) ;
#394=DIRECTION ( 'NONE',  ( -0.000000000000000000, 0.5000000000000003331, -0.8660254037844383745 ) ) ;
#399=ORIENTED_EDGE ( 'NONE', *, *, #2047, .T. ) ;
#400=DIRECTION ( 'NONE',  ( -1.000000000000000000, -0.000000000000000000, -0.000000000000000000 ) ) ;
#401=VERTEX_POINT ( 'NONE', #1491 ) ;
#404=CARTESIAN_POINT ( 'NONE',  ( 0.000000000000000000, 3.490243377569956061E-16, -2.849999999999999645 ) ) ;
#406=ORIENTED_EDGE ( 'NONE', *, *, #733, .T. ) ;
#427=FACE_OUTER_BOUND ( 'NONE', #2786, .T. ) ;
#428=EDGE_LOOP ( 'NONE', ( #2332, #810, #725 ) ) ;
#431=FACE_OUTER_BOUND ( 'NONE', #2490, .T. ) ;
#438=DIRECTION ( 'NONE',  ( -1.000000000000000000, -0.000000000000000000, -0.000000000000000000 ) ) ;
#439=VECTOR ( 'NONE', #888, 1000.000000000000227 ) ;
#445=AXIS2_PLACEMENT_3D ( 'NONE', #594, #3096, #3064 ) ;
#453=CARTESIAN_POINT ( 'NONE',  ( 1.649999999999999911, 3.490243377569956061E-16, -2.849999999999999645 ) ) ;
#454=DIRECTION ( 'NONE',  ( 0.000000000000000000, 0.000000000000000000, 1.000000000000000000 ) ) ;
#456=EDGE_CURVE ( 'NONE', #1944, #79, #2985, .T. ) ;
#460=VECTOR ( 'NONE', #601, 999.9999999999998863 ) ;
#462=AXIS2_PLACEMENT_3D ( 'NONE', #2599, #1915, #160 ) ;
#474=CARTESIAN_POINT ( 'NONE',  ( 1.040000000000000036, 0.5773502691896263972, -1.000000000000000000 ) ) ;
#476=TOROIDAL_SURFACE ( 'NONE', #2813, 1.599999999999999645, 0.1000000000000000056 ) ;
#477=LINE ( 'NONE', #1223, #1086 ) ;
#480=FACE_OUTER_BOUND ( 'NONE', #886, .T. ) ;
#483=FACE_OUTER_BOUND ( 'NONE', #2112, .T. ) ;
#486=DIRECTION ( 'NONE',  ( -1.000000000000000000, 0.000000000000000000, -0.000000000000000000 ) ) ;
#488=VERTEX_POINT ( 'NONE', #1274 ) ;
#490=AXIS2_PLACEMENT_3D ( 'NONE', #3159, #891, #141 ) ;
#496=AXIS2_PLACEMENT_3D ( 'NONE', #1455, #2509, #249 ) ;
#499=PRODUCT_DEFINITION ( 'UNKNOWN', '', #758, #2762 ) ;
#500=ORIENTED_EDGE ( 'NONE', *, *, #591, .T. ) ;
#503=CARTESIAN_POINT ( 'NONE',  ( 7.650000000000000355, 0.000000000000000000, 0.000000000000000000 ) ) ;
#513=ORIENTED_EDGE ( 'NONE', *, *, #2779, .F. ) ;
#517=EDGE_CURVE ( 'NONE', #3213, #1108, #2029, .T. ) ;
#519=DIRECTION ( 'NONE',  ( -0.000000000000000000, 0.5000000000000000000, 0.8660254037844385966 ) ) ;
#520=CARTESIAN_POINT ( 'NONE',  ( 1.269999999999999796, 0.000000000000000000, 0.000000000000000000 ) ) ;
#521=CARTESIAN_POINT ( 'NONE',  ( 1.040000000000000036, 1.154700538379252350, -1.084202172485497162E-16 ) ) ;
#524=SHAPE_REPRESENTATION ( 'socket button head screw_iso_ISO 7380 - M3 x 6 - 6N', ( #2878 ), #1010 ) ;
#534=PLANE ( 'NONE',  #3005 ) ;
#545=CIRCLE ( 'NONE', #2775, 3.351416843938785028 ) ;
#547=CIRCLE ( 'NONE', #2359, 2.849999999999999645 ) ;
#549=VECTOR ( 'NONE', #1448, 1000.000000000000000 ) ;
#550=CIRCLE ( 'NONE', #2314, 1.000000000000000000 ) ;
#555=ORIENTED_EDGE ( 'NONE', *, *, #1912, .F. ) ;
#562=CARTESIAN_POINT ( 'NONE',  ( 0.000000000000000000, -1.154700538379251684, -1.199226976249124676E-17 ) ) ;
#566=EDGE_CURVE ( 'NONE', #914, #391, #2569, .T. ) ;
#568=FACE_OUTER_BOUND ( 'NONE', #2317, .T. ) ;
#569=EDGE_LOOP ( 'NONE', ( #1118, #2896, #1520, #1946, #2140 ) ) ;
#580=CARTESIAN_POINT ( 'NONE',  ( 1.040000000000000036, 0.5773502691896263972, 1.000000000000000000 ) ) ;
#581=EDGE_LOOP ( 'NONE', ( #1628, #2886, #1194 ) ) ;
#588=DIRECTION ( 'NONE',  ( 0.000000000000000000, 0.000000000000000000, -1.000000000000000000 ) ) ;
#591=EDGE_CURVE ( 'NONE', #488, #815, #2290, .T. ) ;
#594=CARTESIAN_POINT ( 'NONE',  ( 7.369500000000001272, 0.000000000000000000, 0.000000000000000000 ) ) ;
#595=STYLED_ITEM('',(#3264),#27);
#601=DIRECTION ( 'NONE',  ( -0.7071067811865472397, 0.000000000000000000, 0.7071067811865479058 ) ) ;
#602=ORIENTED_EDGE ( 'NONE', *, *, #1206, .T. ) ;
#622=CIRCLE ( 'NONE', #2438, 1.219500000000000028 ) ;
#624=EDGE_LOOP ( 'NONE', ( #2555, #789 ) ) ;
#626=VERTEX_POINT ( 'NONE', #1562 ) ;
#628=VERTEX_POINT ( 'NONE', #2005 ) ;
#635=ORIENTED_EDGE ( 'NONE', *, *, #2964, .T. ) ;
#638=LINE ( 'NONE', #3137, #2109 ) ;
#642=APPLICATION_CONTEXT ( 'automotive_design' ) ;
#648=CARTESIAN_POINT ( 'NONE',  ( 7.650000000000000355, 0.000000000000000000, 1.219500000000000028 ) ) ;
#651=ORIENTED_EDGE ( 'NONE', *, *, #2800, .T. ) ;
#658=VERTEX_POINT ( 'NONE', #328 ) ;
#660=EDGE_CURVE ( 'NONE', #1860, #1904, #1813, .T. ) ;
#678=ORIENTED_EDGE ( 'NONE', *, *, #3014, .F. ) ;
#679=PLANE ( 'NONE',  #1059 ) ;
#680=ORIENTED_EDGE ( 'NONE', *, *, #2129, .T. ) ;
#683=DIRECTION ( 'NONE',  ( 0.000000000000000000, 0.000000000000000000, 1.000000000000000000 ) ) ;
#685=DIRECTION ( 'NONE',  ( 0.000000000000000000, 0.000000000000000000, 1.000000000000000000 ) ) ;
#688=AXIS2_PLACEMENT_3D ( 'NONE', #503, #2415, #965 ) ;
#701=AXIS2_PLACEMENT_3D ( 'NONE', #3218, #2792, #1016 ) ;
#706=LINE ( 'NONE', #474, #2158 ) ;
#707=DIRECTION ( 'NONE',  ( -0.000000000000000000, -0.5000000000000000000, 0.8660254037844385966 ) ) ;
#716=DIRECTION ( 'NONE',  ( 0.000000000000000000, 1.000000000000000000, 1.224646799147353207E-16 ) ) ;
#717=DIRECTION ( 'NONE',  ( 0.000000000000000000, 0.000000000000000000, 1.000000000000000000 ) ) ;
#719=DIRECTION ( 'NONE',  ( -1.000000000000000000, 0.000000000000000000, -0.000000000000000000 ) ) ;
#721=EDGE_CURVE ( 'NONE', #1182, #169, #2268, .T. ) ;
#724=CARTESIAN_POINT ( 'NONE',  ( 1.269999999999999796, -2.850000000000000533, -3.490243377569956061E-16 ) ) ;
#725=ORIENTED_EDGE ( 'NONE', *, *, #2852, .F. ) ;
#733=EDGE_CURVE ( 'NONE', #2373, #626, #638, .T. ) ;
#745=VERTEX_POINT ( 'NONE', #154 ) ;
#748=EDGE_CURVE ( 'NONE', #79, #3095, #2563, .T. ) ;
#752=ORIENTED_EDGE ( 'NONE', *, *, #2047, .F. ) ;
#753=ORIENTED_EDGE ( 'NONE', *, *, #1619, .F. ) ;
#758=PRODUCT_DEFINITION_FORMATION_WITH_SPECIFIED_SOURCE ( 'ANY', '', #2237, .NOT_KNOWN. ) ;
#759=EDGE_CURVE ( 'NONE', #626, #2346, #3103, .T. ) ;
#761=EDGE_CURVE ( 'NONE', #3197, #2355, #2875, .T. ) ;
#763=ORIENTED_EDGE ( 'NONE', *, *, #270, .F. ) ;
#765=CARTESIAN_POINT ( 'NONE',  ( 1.649999999999999911, 0.000000000000000000, 0.000000000000000000 ) ) ;
#767=AXIS2_PLACEMENT_3D ( 'NONE', #1954, #2911, #683 ) ;
#780=DIRECTION ( 'NONE',  ( -1.000000000000000000, -0.000000000000000000, -0.000000000000000000 ) ) ;
#786=DIRECTION ( 'NONE',  ( -0.7071067811865472397, 8.659560562354937789E-17, -0.7071067811865479058 ) ) ;
#789=ORIENTED_EDGE ( 'NONE', *, *, #337, .T. ) ;
#791=CARTESIAN_POINT ( 'NONE',  ( 1.750000000000000000, 0.000000000000000000, 0.000000000000000000 ) ) ;
#803=VECTOR ( 'NONE', #2318, 1000.000000000000227 ) ;
#810=ORIENTED_EDGE ( 'NONE', *, *, #517, .F. ) ;
#813=CARTESIAN_POINT ( 'NONE',  ( 1.269999999999999796, 0.000000000000000000, 0.000000000000000000 ) ) ;
#814=CARTESIAN_POINT ( 'NONE',  ( 1.040000000000000036, -1.154700538379251684, 0.000000000000000000 ) ) ;
#815=VERTEX_POINT ( 'NONE', #872 ) ;
#820=DIRECTION ( 'NONE',  ( -0.000000000000000000, -0.5000000000000003331, -0.8660254037844383745 ) ) ;
#821=DIRECTION ( 'NONE',  ( 0.000000000000000000, 0.000000000000000000, 1.000000000000000000 ) ) ;
#822=SURFACE_STYLE_FILL_AREA ( #2068 ) ;
#824=ADVANCED_BREP_SHAPE_REPRESENTATION ( '', ( #27, #2878 ), #1010 ) ;
#830=ORIENTED_EDGE ( 'NONE', *, *, #2211, .T. ) ;
#842=AXIS2_PLACEMENT_3D ( 'NONE', #2187, #3172, #938 ) ;
#844=VECTOR ( 'NONE', #820, 1000.000000000000114 ) ;
#848=CARTESIAN_POINT ( 'NONE',  ( 0.000000000000000000, 0.5773502691896263972, -1.000000000000000000 ) ) ;
#855=ORIENTED_EDGE ( 'NONE', *, *, #1308, .T. ) ;
#857=PLANE ( 'NONE',  #1367 ) ;
#862=ADVANCED_FACE ( 'NONE', ( #2594, #2858 ), #1684, .T. ) ;
#872=CARTESIAN_POINT ( 'NONE',  ( 1.750000000000000000, 0.000000000000000000, 1.499999999999999556 ) ) ;
#885=EDGE_LOOP ( 'NONE', ( #2107, #555, #2207 ) ) ;
#886=EDGE_LOOP ( 'NONE', ( #2902, #3101, #2704, #146, #2952 ) ) ;
#887=CARTESIAN_POINT ( 'NONE',  ( 1.617350269189632428, 0.000000000000000000, 0.000000000000000000 ) ) ;
#888=DIRECTION ( 'NONE',  ( -0.000000000000000000, -0.5000000000000000000, 0.8660254037844385966 ) ) ;
#890=AXIS2_PLACEMENT_3D ( 'NONE', #2030, #2540, #1759 ) ;
#891=DIRECTION ( 'NONE',  ( 0.000000000000000000, -0.8660254037844387076, -0.5000000000000001110 ) ) ;
#892=ORIENTED_EDGE ( 'NONE', *, *, #1433, .T. ) ;
#897=ORIENTED_EDGE ( 'NONE', *, *, #2211, .F. ) ;
#905=ORIENTED_EDGE ( 'NONE', *, *, #1329, .F. ) ;
#914=VERTEX_POINT ( 'NONE', #1705 ) ;
#923=CIRCLE ( 'NONE', #1970, 1.000000000000000000 ) ;
#926=CIRCLE ( 'NONE', #462, 1.599999999999999645 ) ;
#927=EDGE_CURVE ( 'NONE', #1944, #2825, #1216, .T. ) ;
#928=CARTESIAN_POINT ( 'NONE',  ( 1.040000000000000036, -1.154700538379251684, 0.000000000000000000 ) ) ;
#934=CARTESIAN_POINT ( 'NONE',  ( 7.650000000000000355, 0.000000000000000000, 0.000000000000000000 ) ) ;
#935=DIRECTION ( 'NONE',  ( -0.000000000000000000, -1.000000000000000000, -0.000000000000000000 ) ) ;
#936=DIRECTION ( 'NONE',  ( -1.000000000000000000, -0.000000000000000000, -0.000000000000000000 ) ) ;
#938=DIRECTION ( 'NONE',  ( 0.000000000000000000, 0.000000000000000000, 1.000000000000000000 ) ) ;
#947=EDGE_CURVE ( 'NONE', #2850, #815, #2610, .T. ) ;
#948=DIRECTION ( 'NONE',  ( 0.000000000000000000, 0.000000000000000000, 1.000000000000000000 ) ) ;
#950=LINE ( 'NONE', #1211, #1940 ) ;
#956=VECTOR ( 'NONE', #1905, 1000.000000000000000 ) ;
#965=DIRECTION ( 'NONE',  ( 0.000000000000000000, 0.000000000000000000, 1.000000000000000000 ) ) ;
#968=DIRECTION ( 'NONE',  ( 0.000000000000000000, 0.000000000000000000, 1.000000000000000000 ) ) ;
#971=CONICAL_SURFACE ( 'NONE', #2796, 1732.050807568857181, 1.047197551196592746 ) ;
#972=CARTESIAN_POINT ( 'NONE',  ( 0.000000000000000000, 1.836970198721029441E-16, -1.499999999999999556 ) ) ;
#977=DIRECTION ( 'NONE',  ( 0.000000000000000000, -0.5000000000000003331, 0.8660254037844383745 ) ) ;
#988=DIRECTION ( 'NONE',  ( 1.000000000000000000, 0.000000000000000000, -0.000000000000000000 ) ) ;
#996=CARTESIAN_POINT ( 'NONE',  ( 3.033375984251970081, -8.673617379884035472E-16, 0.000000000000000000 ) ) ;
#997=DIRECTION ( 'NONE',  ( 0.000000000000000000, 0.000000000000000000, 1.000000000000000000 ) ) ;
#1001=AXIS2_PLACEMENT_3D ( 'NONE', #791, #1545, #2988 ) ;
#1008=VECTOR ( 'NONE', #351, 1000.000000000000114 ) ;
#1010=( GEOMETRIC_REPRESENTATION_CONTEXT ( 3 ) GLOBAL_UNCERTAINTY_ASSIGNED_CONTEXT ( ( #2860 ) ) GLOBAL_UNIT_ASSIGNED_CONTEXT ( ( #2794, #2764, #1312 ) ) REPRESENTATION_CONTEXT ( 'NONE', 'WORKASPACE' ) );
#1013=CARTESIAN_POINT ( 'NONE',  ( 1.617350269189632428, 0.000000000000000000, 0.000000000000000000 ) ) ;
#1014=PLANE ( 'NONE',  #890 ) ;
#1016=DIRECTION ( 'NONE',  ( -0.000000000000000000, 0.000000000000000000, -1.000000000000000000 ) ) ;
#1019=CARTESIAN_POINT ( 'NONE',  ( 0.000000000000000000, 0.000000000000000000, 2.849999999999999645 ) ) ;
#1022=ADVANCED_FACE ( 'NONE', ( #171 ), #221, .T. ) ;
#1023=VERTEX_POINT ( 'NONE', #2929 ) ;
#1034=ADVANCED_FACE ( 'NONE', ( #3206 ), #2711, .F. ) ;
#1035=DIRECTION ( 'NONE',  ( -1.000000000000000000, 0.000000000000000000, 0.000000000000000000 ) ) ;
#1042=FACE_OUTER_BOUND ( 'NONE', #885, .T. ) ;
#1043=ORIENTED_EDGE ( 'NONE', *, *, #257, .T. ) ;
#1044=EDGE_CURVE ( 'NONE', #1890, #79, #1895, .T. ) ;
#1059=AXIS2_PLACEMENT_3D ( 'NONE', #2007, #2907, #1933 ) ;
#1063=CARTESIAN_POINT ( 'NONE',  ( 7.369500000000001272, 1.836970198721029934E-16, -1.500000000000000000 ) ) ;
#1074=CIRCLE ( 'NONE', #2330, 2.849999999999999645 ) ;
#1078=CARTESIAN_POINT ( 'NONE',  ( 1.750000000000000000, 1.959434878635764737E-16, -1.599999999999999645 ) ) ;
#1086=VECTOR ( 'NONE', #3210, 1000.000000000000000 ) ;
#1090=ORIENTED_EDGE ( 'NONE', *, *, #2497, .T. ) ;
#1093=CARTESIAN_POINT ( 'NONE',  ( 1.649999999999999911, 0.000000000000000000, 0.000000000000000000 ) ) ;
#1096=EDGE_LOOP ( 'NONE', ( #1090, #855, #1208, #2383, #406, #2169 ) ) ;
#1108=VERTEX_POINT ( 'NONE', #291 ) ;
#1112=VECTOR ( 'NONE', #2342, 1000.000000000000000 ) ;
#1118=ORIENTED_EDGE ( 'NONE', *, *, #927, .F. ) ;
#1123=FACE_OUTER_BOUND ( 'NONE', #428, .T. ) ;
#1125=UNCERTAINTY_MEASURE_WITH_UNIT (LENGTH_MEASURE( 1.000000000000000082E-05 ), #348, 'distance_accuracy_value', 'NONE');
#1126=CARTESIAN_POINT ( 'NONE',  ( 4.336808689942017736E-16, 0.000000000000000000, 0.000000000000000000 ) ) ;
#1136=DIRECTION ( 'NONE',  ( 0.000000000000000000, 0.000000000000000000, 1.000000000000000000 ) ) ;
#1140=DIRECTION ( 'NONE',  ( -0.000000000000000000, 0.000000000000000000, -1.000000000000000000 ) ) ;
#1145=ORIENTED_EDGE ( 'NONE', *, *, #1361, .F. ) ;
#1151=CIRCLE ( 'NONE', #1985, 2.849999999999999645 ) ;
#1153=CARTESIAN_POINT ( 'NONE',  ( 1.269999999999999796, 0.000000000000000000, 0.000000000000000000 ) ) ;
#1154=CARTESIAN_POINT ( 'NONE',  ( 1.040000000000000036, 0.5773502691896263972, -1.000000000000000000 ) ) ;
#1158=ORIENTED_EDGE ( 'NONE', *, *, #2761, .T. ) ;
#1159=FACE_BOUND ( 'NONE', #624, .T. ) ;
#1168=CIRCLE ( 'NONE', #2674, 0.1000000000000000472 ) ;
#1174=ADVANCED_FACE ( 'NONE', ( #3082 ), #1649, .T. ) ;
#1175=MECHANICAL_DESIGN_GEOMETRIC_PRESENTATION_REPRESENTATION('',(#2677),#3200);
#1178=VERTEX_POINT ( 'NONE', #2337 ) ;
#1181=DIRECTION ( 'NONE',  ( -1.000000000000000000, -0.000000000000000000, -0.000000000000000000 ) ) ;
#1182=VERTEX_POINT ( 'NONE', #2837 ) ;
#1183=FACE_OUTER_BOUND ( 'NONE', #2367, .T. ) ;
#1185=DIRECTION ( 'NONE',  ( 0.000000000000000000, 0.000000000000000000, 1.000000000000000000 ) ) ;
#1186=DIRECTION ( 'NONE',  ( -1.000000000000000000, -0.000000000000000000, -0.000000000000000000 ) ) ;
#1191=CARTESIAN_POINT ( 'NONE',  ( 1.040000000000000036, 1.154700538379252350, -1.084202172485497162E-16 ) ) ;
#1194=ORIENTED_EDGE ( 'NONE', *, *, #2761, .F. ) ;
#1197=LINE ( 'NONE', #2196, #2973 ) ;
#1204=CONICAL_SURFACE ( 'NONE', #377, 1732.050807568857181, 1.047197551196592746 ) ;
#1205=CARTESIAN_POINT ( 'NONE',  ( 1.040000000000000036, 0.8660254037844390407, -0.5000000000000002220 ) ) ;
#1206=EDGE_CURVE ( 'NONE', #658, #2850, #2177, .T. ) ;
#1208=ORIENTED_EDGE ( 'NONE', *, *, #761, .T. ) ;
#1209=FACE_OUTER_BOUND ( 'NONE', #1575, .T. ) ;
#1211=CARTESIAN_POINT ( 'NONE',  ( 1.040000000000000036, -1.154700538379251684, -1.199226976249124676E-17 ) ) ;
#1213=VECTOR ( 'NONE', #394, 1000.000000000000114 ) ;
#1216=LINE ( 'NONE', #2947, #3135 ) ;
#1218=CIRCLE ( 'NONE', #2724, 1.000000000000000000 ) ;
#1223=CARTESIAN_POINT ( 'NONE',  ( 1.040000000000000036, 0.5773502691896263972, -1.000000000000000000 ) ) ;
#1227=EDGE_CURVE ( 'NONE', #391, #628, #923, .T. ) ;
#1231=CARTESIAN_POINT ( 'NONE',  ( 1.040000000000000036, 0.000000000000000000, 0.000000000000000000 ) ) ;
#1240=LINE ( 'NONE', #2986, #1735 ) ;
#1241=CARTESIAN_POINT ( 'NONE',  ( 1.040000000000000036, -1.154700538379251684, 0.000000000000000000 ) ) ;
#1243=EDGE_CURVE ( 'NONE', #745, #488, #2809, .T. ) ;
#1251=DIRECTION ( 'NONE',  ( -1.000000000000000000, -0.000000000000000000, -0.000000000000000000 ) ) ;
#1256=DIRECTION ( 'NONE',  ( -1.000000000000000000, -0.000000000000000000, -0.000000000000000000 ) ) ;
#1261=ORIENTED_EDGE ( 'NONE', *, *, #1734, .T. ) ;
#1268=CARTESIAN_POINT ( 'NONE',  ( 1.040000000000000036, 0.000000000000000000, 0.000000000000000000 ) ) ;
#1274=CARTESIAN_POINT ( 'NONE',  ( 7.369500000000001272, 0.000000000000000000, 1.499999999999999778 ) ) ;
#1285=AXIS2_PLACEMENT_3D ( 'NONE', #1078, #369, #1822 ) ;
#1289=ORIENTED_EDGE ( 'NONE', *, *, #2593, .T. ) ;
#1291=DIRECTION ( 'NONE',  ( 0.000000000000000000, 0.000000000000000000, -1.000000000000000000 ) ) ;
#1297=ORIENTED_EDGE ( 'NONE', *, *, #2619, .F. ) ;
#1301=CARTESIAN_POINT ( 'NONE',  ( 3.033375984251970081, -8.673617379884035472E-16, 0.000000000000000000 ) ) ;
#1305=CARTESIAN_POINT ( 'NONE',  ( 1.750000000000000000, 1.836970198721029441E-16, -1.499999999999999556 ) ) ;
#1307=ORIENTED_EDGE ( 'NONE', *, *, #3093, .T. ) ;
#1308=EDGE_CURVE ( 'NONE', #1904, #3197, #2853, .T. ) ;
#1312=( NAMED_UNIT ( * ) SI_UNIT ( $, .STERADIAN. ) SOLID_ANGLE_UNIT ( ) );
#1329=EDGE_CURVE ( 'NONE', #1182, #2676, #1667, .T. ) ;
#1334=AXIS2_PLACEMENT_3D ( 'NONE', #1407, #2697, #2401 ) ;
#1339=EDGE_LOOP ( 'NONE', ( #905, #3083 ) ) ;
#1341=DIRECTION ( 'NONE',  ( -1.000000000000000000, -0.000000000000000000, -0.000000000000000000 ) ) ;
#1345=ADVANCED_FACE ( 'NONE', ( #2387 ), #971, .F. ) ;
#1346=CARTESIAN_POINT ( 'NONE',  ( 0.000000000000000000, -0.5773502691896253980, -1.000000000000000000 ) ) ;
#1349=ORIENTED_EDGE ( 'NONE', *, *, #2110, .T. ) ;
#1353=CARTESIAN_POINT ( 'NONE',  ( 1.040000000000000036, -0.5773502691896253980, -1.000000000000000000 ) ) ;
#1356=AXIS2_PLACEMENT_3D ( 'NONE', #1456, #202, #1936 ) ;
#1361=EDGE_CURVE ( 'NONE', #1849, #1023, #2235, .T. ) ;
#1367=AXIS2_PLACEMENT_3D ( 'NONE', #928, #1397, #1140 ) ;
#1370=CARTESIAN_POINT ( 'NONE',  ( 1.040000000000000036, -1.154700538379251684, -1.199226976249124676E-17 ) ) ;
#1373=AXIS2_PLACEMENT_3D ( 'NONE', #765, #2227, #265 ) ;
#1377=ORIENTED_EDGE ( 'NONE', *, *, #1797, .T. ) ;
#1384=CARTESIAN_POINT ( 'NONE',  ( 1.040000000000000036, -1.154700538379251684, 0.000000000000000000 ) ) ;
#1387=ORIENTED_EDGE ( 'NONE', *, *, #1361, .T. ) ;
#1397=DIRECTION ( 'NONE',  ( 1.000000000000000000, 0.000000000000000000, -0.000000000000000000 ) ) ;
#1398=ORIENTED_EDGE ( 'NONE', *, *, #1308, .F. ) ;
#1402=ORIENTED_EDGE ( 'NONE', *, *, #3037, .F. ) ;
#1404=DIRECTION ( 'NONE',  ( -1.000000000000000000, -0.000000000000000000, -0.000000000000000000 ) ) ;
#1407=CARTESIAN_POINT ( 'NONE',  ( 4.336808689942017736E-16, 0.000000000000000000, 0.000000000000000000 ) ) ;
#1414=CARTESIAN_POINT ( 'NONE',  ( 1.040000000000000036, 1.154700538379252350, -1.084202172485497162E-16 ) ) ;
#1418=DIRECTION ( 'NONE',  ( 0.000000000000000000, -1.000000000000000000, 0.000000000000000000 ) ) ;
#1421=LINE ( 'NONE', #3201, #956 ) ;
#1433=EDGE_CURVE ( 'NONE', #1023, #1694, #1609, .T. ) ;
#1438=CARTESIAN_POINT ( 'NONE',  ( 1.040000000000000036, -1.154700538379251684, -1.199226976249124676E-17 ) ) ;
#1446=EDGE_CURVE ( 'NONE', #2348, #745, #622, .T. ) ;
#1448=DIRECTION ( 'NONE',  ( -1.000000000000000000, -0.000000000000000000, -0.000000000000000000 ) ) ;
#1455=CARTESIAN_POINT ( 'NONE',  ( 7.369500000000001272, 0.000000000000000000, 0.000000000000000000 ) ) ;
#1456=CARTESIAN_POINT ( 'NONE',  ( 1.750000000000000000, 0.000000000000000000, 0.000000000000000000 ) ) ;
#1460=DIRECTION ( 'NONE',  ( 0.000000000000000000, 0.000000000000000000, 1.000000000000000000 ) ) ;
#1463=EDGE_CURVE ( 'NONE', #2676, #1182, #2899, .T. ) ;
#1465=VECTOR ( 'NONE', #214, 1000.000000000000000 ) ;
#1468=EDGE_LOOP ( 'NONE', ( #2834, #2398, #1884, #1349, #283 ) ) ;
#1477=AXIS2_PLACEMENT_3D ( 'NONE', #1301, #588, #2073 ) ;
#1491=CARTESIAN_POINT ( 'NONE',  ( 1.269999999999999796, 3.490243377569956061E-16, -2.849999999999999645 ) ) ;
#1498=AXIS2_PLACEMENT_3D ( 'NONE', #2352, #1341, #2870 ) ;
#1502=CARTESIAN_POINT ( 'NONE',  ( 1.040000000000000036, -1.154700538379251684, 0.000000000000000000 ) ) ;
#1506=LINE ( 'NONE', #2244, #2550 ) ;
#1513=AXIS2_PLACEMENT_3D ( 'NONE', #813, #3050, #138 ) ;
#1519=CIRCLE ( 'NONE', #1356, 1.499999999999999556 ) ;
#1520=ORIENTED_EDGE ( 'NONE', *, *, #2006, .T. ) ;
#1522=FACE_OUTER_BOUND ( 'NONE', #2096, .T. ) ;
#1529=AXIS2_PLACEMENT_3D ( 'NONE', #1414, #175, #2173 ) ;
#1535=AXIS2_PLACEMENT_3D ( 'NONE', #2789, #1291, #1818 ) ;
#1539=ORIENTED_EDGE ( 'NONE', *, *, #591, .F. ) ;
#1545=DIRECTION ( 'NONE',  ( -1.000000000000000000, -0.000000000000000000, -0.000000000000000000 ) ) ;
#1556=CARTESIAN_POINT ( 'NONE',  ( 1.040000000000000036, -0.5773502691896253980, -1.000000000000000000 ) ) ;
#1559=DIRECTION ( 'NONE',  ( 0.000000000000000000, 0.000000000000000000, -1.000000000000000000 ) ) ;
#1562=CARTESIAN_POINT ( 'NONE',  ( 0.000000000000000000, 1.154700538379252350, -1.084202172485497162E-16 ) ) ;
#1564=ADVANCED_FACE ( 'NONE', ( #1042 ), #534, .F. ) ;
#1574=SURFACE_STYLE_USAGE ( .BOTH. , #2810 ) ;
#1575=EDGE_LOOP ( 'NONE', ( #2542, #635, #651, #1398, #152 ) ) ;
#1582=( GEOMETRIC_REPRESENTATION_CONTEXT ( 3 ) GLOBAL_UNCERTAINTY_ASSIGNED_CONTEXT ( ( #1125 ) ) GLOBAL_UNIT_ASSIGNED_CONTEXT ( ( #348, #2288, #2041 ) ) REPRESENTATION_CONTEXT ( 'NONE', 'WORKASPACE' ) );
#1583=DIRECTION ( 'NONE',  ( -0.000000000000000000, 0.000000000000000000, -1.000000000000000000 ) ) ;
#1584=VECTOR ( 'NONE', #2573, 1000.000000000000114 ) ;
#1592=LINE ( 'NONE', #1353, #1584 ) ;
#1598=PLANE ( 'NONE',  #490 ) ;
#1609=CIRCLE ( 'NONE', #1334, 1.425000000000000044 ) ;
#1612=DIRECTION ( 'NONE',  ( 0.000000000000000000, 0.000000000000000000, 1.000000000000000000 ) ) ;
#1619=EDGE_CURVE ( 'NONE', #373, #401, #1074, .T. ) ;
#1628=ORIENTED_EDGE ( 'NONE', *, *, #2308, .F. ) ;
#1649=CYLINDRICAL_SURFACE ( 'NONE', #1498, 2.849999999999999645 ) ;
#1651=( NAMED_UNIT ( * ) PLANE_ANGLE_UNIT ( ) SI_UNIT ( $, .RADIAN. ) );
#1653=DIRECTION ( 'NONE',  ( -1.000000000000000000, -0.000000000000000000, -0.000000000000000000 ) ) ;
#1657=CARTESIAN_POINT ( 'NONE',  ( 3.033375984251970081, -8.673617379884035472E-16, 0.000000000000000000 ) ) ;
#1663=ADVANCED_FACE ( 'NONE', ( #568 ), #2396, .F. ) ;
#1666=DIRECTION ( 'NONE',  ( 0.000000000000000000, 0.000000000000000000, 1.000000000000000000 ) ) ;
#1667=CIRCLE ( 'NONE', #201, 2.849999999999999645 ) ;
#1674=DIRECTION ( 'NONE',  ( 1.000000000000000000, 0.000000000000000000, -0.000000000000000000 ) ) ;
#1684=PLANE ( 'NONE',  #2665 ) ;
#1694=VERTEX_POINT ( 'NONE', #2904 ) ;
#1695=VECTOR ( 'NONE', #2635, 1000.000000000000000 ) ;
#1698=VECTOR ( 'NONE', #1961, 1000.000000000000000 ) ;
#1700=DIRECTION ( 'NONE',  ( 0.000000000000000000, 0.000000000000000000, 1.000000000000000000 ) ) ;
#1701=EDGE_CURVE ( 'NONE', #1756, #658, #926, .T. ) ;
#1703=VECTOR ( 'NONE', #780, 1000.000000000000000 ) ;
#1705=CARTESIAN_POINT ( 'NONE',  ( 1.040000000000000036, -1.154700538379251684, -1.199226976249124676E-17 ) ) ;
#1710=FACE_OUTER_BOUND ( 'NONE', #1339, .T. ) ;
#1722=LINE ( 'NONE', #972, #549 ) ;
#1733=CARTESIAN_POINT ( 'NONE',  ( 1.040000000000000036, -0.5773502691896253980, -1.000000000000000000 ) ) ;
#1734=EDGE_CURVE ( 'NONE', #1694, #1023, #1765, .T. ) ;
#1735=VECTOR ( 'NONE', #519, 1000.000000000000227 ) ;
#1737=ORIENTED_EDGE ( 'NONE', *, *, #2864, .F. ) ;
#1738=EDGE_LOOP ( 'NONE', ( #2568, #680, #1387, #3125, #49 ) ) ;
#1756=VERTEX_POINT ( 'NONE', #2638 ) ;
#1759=DIRECTION ( 'NONE',  ( 1.000000000000000000, 0.000000000000000000, -0.000000000000000000 ) ) ;
#1761=FACE_OUTER_BOUND ( 'NONE', #352, .T. ) ;
#1765=CIRCLE ( 'NONE', #2845, 1.425000000000000044 ) ;
#1771=ORIENTED_EDGE ( 'NONE', *, *, #220, .T. ) ;
#1772=EDGE_CURVE ( 'NONE', #1108, #1178, #261, .T. ) ;
#1780=AXIS2_PLACEMENT_3D ( 'NONE', #2535, #2039, #1612 ) ;
#1786=CARTESIAN_POINT ( 'NONE',  ( 0.000000000000000000, 0.000000000000000000, 1.499999999999999556 ) ) ;
#1791=DIRECTION ( 'NONE',  ( -0.000000000000000000, 0.5000000000000000000, 0.8660254037844385966 ) ) ;
#1797=EDGE_CURVE ( 'NONE', #745, #2348, #155, .T. ) ;
#1801=VECTOR ( 'NONE', #2333, 1000.000000000000114 ) ;
#1805=DIRECTION ( 'NONE',  ( 0.000000000000000000, 0.000000000000000000, 1.000000000000000000 ) ) ;
#1813=LINE ( 'NONE', #2766, #2565 ) ;
#1818=DIRECTION ( 'NONE',  ( -1.000000000000000000, 0.000000000000000000, -0.000000000000000000 ) ) ;
#1820=CARTESIAN_POINT ( 'NONE',  ( 1.269999999999999796, 0.000000000000000000, 0.000000000000000000 ) ) ;
#1822=DIRECTION ( 'NONE',  ( 0.000000000000000000, -1.224646799147353207E-16, 1.000000000000000000 ) ) ;
#1832=EDGE_LOOP ( 'NONE', ( #1145, #399, #2048, #117, #316 ) ) ;
#1833=DIRECTION ( 'NONE',  ( 0.000000000000000000, 0.000000000000000000, 1.000000000000000000 ) ) ;
#1835=EDGE_LOOP ( 'NONE', ( #2410, #2151, #1307, #3160 ) ) ;
#1837=DIRECTION ( 'NONE',  ( 1.000000000000000000, 0.000000000000000000, 0.000000000000000000 ) ) ;
#1841=PLANE ( 'NONE',  #3081 ) ;
#1845=ADVANCED_FACE ( 'NONE', ( #2254 ), #9, .F. ) ;
#1849=VERTEX_POINT ( 'NONE', #724 ) ;
#1850=APPLICATION_CONTEXT ( 'automotive_design' ) ;
#1854=( LENGTH_UNIT ( ) NAMED_UNIT ( * ) SI_UNIT ( .MILLI., .METRE. ) );
#1856=ORIENTED_EDGE ( 'NONE', *, *, #947, .T. ) ;
#1860=VERTEX_POINT ( 'NONE', #2009 ) ;
#1863=AXIS2_PLACEMENT_3D ( 'NONE', #1384, #1674, #3108 ) ;
#1871=EDGE_LOOP ( 'NONE', ( #2504, #602, #513, #2804 ) ) ;
#1884=ORIENTED_EDGE ( 'NONE', *, *, #3136, .T. ) ;
#1885=CARTESIAN_POINT ( 'NONE',  ( 0.000000000000000000, 0.5773502691896263972, 1.000000000000000000 ) ) ;
#1890=VERTEX_POINT ( 'NONE', #1205 ) ;
#1895=CIRCLE ( 'NONE', #2357, 1.000000000000000000 ) ;
#1904=VERTEX_POINT ( 'NONE', #2458 ) ;
#1905=DIRECTION ( 'NONE',  ( -0.000000000000000000, -1.000000000000000000, -0.000000000000000000 ) ) ;
#1912=EDGE_CURVE ( 'NONE', #2818, #79, #477, .T. ) ;
#1915=DIRECTION ( 'NONE',  ( -1.000000000000000000, -0.000000000000000000, -0.000000000000000000 ) ) ;
#1927=DIRECTION ( 'NONE',  ( -0.5000000000000042188, 0.000000000000000000, 0.8660254037844361541 ) ) ;
#1933=DIRECTION ( 'NONE',  ( -0.000000000000000000, 0.000000000000000000, 1.000000000000000000 ) ) ;
#1936=DIRECTION ( 'NONE',  ( 0.000000000000000000, 0.000000000000000000, 1.000000000000000000 ) ) ;
#1940=VECTOR ( 'NONE', #3203, 1000.000000000000000 ) ;
#1944=VERTEX_POINT ( 'NONE', #887 ) ;
#1945=DIRECTION ( 'NONE',  ( 0.000000000000000000, 0.000000000000000000, -1.000000000000000000 ) ) ;
#1946=ORIENTED_EDGE ( 'NONE', *, *, #1227, .T. ) ;
#1949=LINE ( 'NONE', #404, #1465 ) ;
#1954=CARTESIAN_POINT ( 'NONE',  ( 1.649999999999999911, 0.000000000000000000, 0.000000000000000000 ) ) ;
#1955=CIRCLE ( 'NONE', #445, 1.499999999999999778 ) ;
#1956=CIRCLE ( 'NONE', #1373, 1.599999999999999645 ) ;
#1960=ADVANCED_FACE ( 'NONE', ( #2632 ), #2841, .T. ) ;
#1961=DIRECTION ( 'NONE',  ( -1.000000000000000000, 0.000000000000000000, 0.000000000000000000 ) ) ;
#1963=ORIENTED_EDGE ( 'NONE', *, *, #1243, .T. ) ;
#1970=AXIS2_PLACEMENT_3D ( 'NONE', #93, #342, #821 ) ;
#1983=AXIS2_PLACEMENT_3D ( 'NONE', #1502, #988, #2717 ) ;
#1985=AXIS2_PLACEMENT_3D ( 'NONE', #1153, #1186, #1460 ) ;
#1998=AXIS2_PLACEMENT_3D ( 'NONE', #239, #486, #2471 ) ;
#2005=CARTESIAN_POINT ( 'NONE',  ( 1.040000000000000036, -0.8660254037844382635, 0.5000000000000002220 ) ) ;
#2006=EDGE_CURVE ( 'NONE', #79, #391, #45, .T. ) ;
#2007=CARTESIAN_POINT ( 'NONE',  ( 1.649999999999999911, 1.499999999999999112, 0.000000000000000000 ) ) ;
#2009=CARTESIAN_POINT ( 'NONE',  ( 1.040000000000000036, -0.5773502691896253980, 1.000000000000000000 ) ) ;
#2012=ORIENTED_EDGE ( 'NONE', *, *, #3136, .F. ) ;
#2015=DIRECTION ( 'NONE',  ( 0.000000000000000000, 0.000000000000000000, 1.000000000000000000 ) ) ;
#2020=AXIS2_PLACEMENT_3D ( 'NONE', #3186, #203, #716 ) ;
#2029=LINE ( 'NONE', #334, #803 ) ;
#2030=CARTESIAN_POINT ( 'NONE',  ( 1.040000000000000036, 0.5773502691896263972, -1.000000000000000000 ) ) ;
#2034=DIRECTION ( 'NONE',  ( 0.000000000000000000, 1.000000000000000000, 0.000000000000000000 ) ) ;
#2039=DIRECTION ( 'NONE',  ( -1.000000000000000000, -0.000000000000000000, -0.000000000000000000 ) ) ;
#2041=( NAMED_UNIT ( * ) SI_UNIT ( $, .STERADIAN. ) SOLID_ANGLE_UNIT ( ) );
#2047=EDGE_CURVE ( 'NONE', #1849, #169, #3120, .T. ) ;
#2048=ORIENTED_EDGE ( 'NONE', *, *, #2489, .T. ) ;
#2057=CARTESIAN_POINT ( 'NONE',  ( 1.040000000000000036, 1.154700538379252350, -1.084202172485497162E-16 ) ) ;
#2064=FACE_OUTER_BOUND ( 'NONE', #569, .T. ) ;
#2068=FILL_AREA_STYLE ('',( #292 ) ) ;
#2069=EDGE_LOOP ( 'NONE', ( #2311, #2475, #2472, #199, #336 ) ) ;
#2073=DIRECTION ( 'NONE',  ( 0.000000000000000000, 1.000000000000000000, 0.000000000000000000 ) ) ;
#2083=DIRECTION ( 'NONE',  ( -0.000000000000000000, 0.5000000000000000000, 0.8660254037844385966 ) ) ;
#2094=DIRECTION ( 'NONE',  ( -1.000000000000000000, -0.000000000000000000, -0.000000000000000000 ) ) ;
#2096=EDGE_LOOP ( 'NONE', ( #1289, #1158, #3023, #2650, #1402 ) ) ;
#2104=ADVANCED_FACE ( 'NONE', ( #3154 ), #476, .F. ) ;
#2107=ORIENTED_EDGE ( 'NONE', *, *, #2006, .F. ) ;
#2109=VECTOR ( 'NONE', #2083, 1000.000000000000227 ) ;
#2110=EDGE_CURVE ( 'NONE', #1108, #1890, #157, .T. ) ;
#2112=EDGE_LOOP ( 'NONE', ( #1737, #384, #1963, #2848 ) ) ;
#2113=LINE ( 'NONE', #1370, #1008 ) ;
#2121=CARTESIAN_POINT ( 'NONE',  ( 0.000000000000000000, 0.5773502691896263972, 1.000000000000000000 ) ) ;
#2122=DIRECTION ( 'NONE',  ( 1.000000000000000000, 0.000000000000000000, 0.000000000000000000 ) ) ;
#2123=ORIENTED_EDGE ( 'NONE', *, *, #3014, .T. ) ;
#2129=EDGE_CURVE ( 'NONE', #401, #1849, #1151, .T. ) ;
#2133=EDGE_LOOP ( 'NONE', ( #1261, #892 ) ) ;
#2140=ORIENTED_EDGE ( 'NONE', *, *, #2308, .T. ) ;
#2142=DIRECTION ( 'NONE',  ( 0.000000000000000000, 0.000000000000000000, 1.000000000000000000 ) ) ;
#2149=PRODUCT_CONTEXT ( 'NONE', #642, 'mechanical' ) ;
#2151=ORIENTED_EDGE ( 'NONE', *, *, #1701, .F. ) ;
#2158=VECTOR ( 'NONE', #2931, 1000.000000000000000 ) ;
#2169=ORIENTED_EDGE ( 'NONE', *, *, #759, .T. ) ;
#2171=CARTESIAN_POINT ( 'NONE',  ( 2.168404344971008868E-16, 0.000000000000000000, 0.000000000000000000 ) ) ;
#2173=DIRECTION ( 'NONE',  ( 0.000000000000000000, -0.5000000000000000000, -0.8660254037844385966 ) ) ;
#2177=CIRCLE ( 'NONE', #1285, 0.1000000000000000472 ) ;
#2187=CARTESIAN_POINT ( 'NONE',  ( 0.000000000000000000, 0.000000000000000000, 0.000000000000000000 ) ) ;
#2189=LINE ( 'NONE', #1733, #2934 ) ;
#2196=CARTESIAN_POINT ( 'NONE',  ( 1.040000000000000036, -0.5773502691896253980, 1.000000000000000000 ) ) ;
#2207=ORIENTED_EDGE ( 'NONE', *, *, #2440, .F. ) ;
#2211=EDGE_CURVE ( 'NONE', #3095, #1890, #35, .T. ) ;
#2219=AXIS2_PLACEMENT_3D ( 'NONE', #934, #3167, #1666 ) ;
#2225=ORIENTED_EDGE ( 'NONE', *, *, #2619, .T. ) ;
#2227=DIRECTION ( 'NONE',  ( -1.000000000000000000, -0.000000000000000000, -0.000000000000000000 ) ) ;
#2230=ADVANCED_FACE ( 'NONE', ( #2294 ), #50, .T. ) ;
#2232=ADVANCED_FACE ( 'NONE', ( #2234 ), #2880, .F. ) ;
#2234=FACE_OUTER_BOUND ( 'NONE', #1835, .T. ) ;
#2235=CIRCLE ( 'NONE', #2020, 3.351416843938785028 ) ;
#2236=CARTESIAN_POINT ( 'NONE',  ( 1.750000000000000000, 0.000000000000000000, 0.000000000000000000 ) ) ;
#2237=PRODUCT ( 'socket button head screw_iso_ISO 7380 - M3 x 6 - 6N', 'socket button head screw_iso_ISO 7380 - M3 x 6 - 6N', '', ( #2149 ) ) ;
#2244=CARTESIAN_POINT ( 'NONE',  ( 7.650000000000000355, 1.493456771560197319E-16, -1.219500000000000028 ) ) ;
#2254=FACE_OUTER_BOUND ( 'NONE', #581, .T. ) ;
#2265=VECTOR ( 'NONE', #2384, 1000.000000000000000 ) ;
#2268=LINE ( 'NONE', #1019, #1703 ) ;
#2270=ADVANCED_FACE ( 'NONE', ( #1761 ), #2496, .F. ) ;
#2275=FACE_OUTER_BOUND ( 'NONE', #2577, .T. ) ;
#2288=( NAMED_UNIT ( * ) PLANE_ANGLE_UNIT ( ) SI_UNIT ( $, .RADIAN. ) );
#2289=ORIENTED_EDGE ( 'NONE', *, *, #2129, .F. ) ;
#2290=LINE ( 'NONE', #1786, #2882 ) ;
#2294=FACE_OUTER_BOUND ( 'NONE', #1832, .T. ) ;
#2297=ORIENTED_EDGE ( 'NONE', *, *, #2864, .T. ) ;
#2305=PLANE ( 'NONE',  #1535 ) ;
#2308=EDGE_CURVE ( 'NONE', #628, #2825, #1218, .T. ) ;
#2311=ORIENTED_EDGE ( 'NONE', *, *, #517, .T. ) ;
#2314=AXIS2_PLACEMENT_3D ( 'NONE', #1268, #2654, #3180 ) ;
#2317=EDGE_LOOP ( 'NONE', ( #75, #131, #162 ) ) ;
#2318=DIRECTION ( 'NONE',  ( -0.000000000000000000, -0.5000000000000000000, 0.8660254037844385966 ) ) ;
#2320=ORIENTED_EDGE ( 'NONE', *, *, #721, .F. ) ;
#2330=AXIS2_PLACEMENT_3D ( 'NONE', #520, #1256, #2015 ) ;
#2332=ORIENTED_EDGE ( 'NONE', *, *, #2110, .F. ) ;
#2333=DIRECTION ( 'NONE',  ( -0.000000000000000000, 0.5000000000000003331, -0.8660254037844383745 ) ) ;
#2337=CARTESIAN_POINT ( 'NONE',  ( 1.040000000000000036, 0.5773502691896263972, 1.000000000000000000 ) ) ;
#2341=ORIENTED_EDGE ( 'NONE', *, *, #2852, .T. ) ;
#2342=DIRECTION ( 'NONE',  ( -0.000000000000000000, 1.000000000000000000, -0.000000000000000000 ) ) ;
#2344=AXIS2_PLACEMENT_3D ( 'NONE', #2738, #1251, #244 ) ;
#2346=VERTEX_POINT ( 'NONE', #1885 ) ;
#2347=AXIS2_PLACEMENT_3D ( 'NONE', #1438, #2431, #200 ) ;
#2348=VERTEX_POINT ( 'NONE', #2351 ) ;
#2349=LINE ( 'NONE', #580, #2265 ) ;
#2351=CARTESIAN_POINT ( 'NONE',  ( 7.650000000000000355, 1.665213485140613626E-16, -1.219500000000000028 ) ) ;
#2352=CARTESIAN_POINT ( 'NONE',  ( 0.000000000000000000, 0.000000000000000000, 0.000000000000000000 ) ) ;
#2353=SHAPE_REPRESENTATION_RELATIONSHIP ( 'NONE' , 'NONE' ,  #524, #824 ) ;
#2355=VERTEX_POINT ( 'NONE', #111 ) ;
#2357=AXIS2_PLACEMENT_3D ( 'NONE', #1231, #3220, #997 ) ;
#2359=AXIS2_PLACEMENT_3D ( 'NONE', #1820, #1404, #948 ) ;
#2366=COLOUR_RGB ( '',1.000000000000000000, 0.9490196078431372140, 0.9098039215686274384 ) ;
#2367=EDGE_LOOP ( 'NONE', ( #1377, #2297, #678, #2369 ) ) ;
#2369=ORIENTED_EDGE ( 'NONE', *, *, #1243, .F. ) ;
#2373=VERTEX_POINT ( 'NONE', #848 ) ;
#2378=CARTESIAN_POINT ( 'NONE',  ( 1.040000000000000036, 0.000000000000000000, -1.000000000000000000 ) ) ;
#2383=ORIENTED_EDGE ( 'NONE', *, *, #151, .T. ) ;
#2384=DIRECTION ( 'NONE',  ( -1.000000000000000000, 0.000000000000000000, 0.000000000000000000 ) ) ;
#2387=FACE_OUTER_BOUND ( 'NONE', #1468, .T. ) ;
#2396=PLANE ( 'NONE',  #1863 ) ;
#2398=ORIENTED_EDGE ( 'NONE', *, *, #927, .T. ) ;
#2401=DIRECTION ( 'NONE',  ( 0.000000000000000000, 0.000000000000000000, 1.000000000000000000 ) ) ;
#2407=CARTESIAN_POINT ( 'NONE',  ( 1.269999999999999796, 0.000000000000000000, 2.849999999999999645 ) ) ;
#2410=ORIENTED_EDGE ( 'NONE', *, *, #1206, .F. ) ;
#2415=DIRECTION ( 'NONE',  ( -1.000000000000000000, -0.000000000000000000, -0.000000000000000000 ) ) ;
#2419=DIRECTION ( 'NONE',  ( -0.000000000000000000, 0.000000000000000000, 1.000000000000000000 ) ) ;
#2431=DIRECTION ( 'NONE',  ( 0.000000000000000000, 0.8660254037844384856, -0.5000000000000004441 ) ) ;
#2438=AXIS2_PLACEMENT_3D ( 'NONE', #2682, #3170, #454 ) ;
#2440=EDGE_CURVE ( 'NONE', #391, #2818, #1592, .T. ) ;
#2445=CYLINDRICAL_SURFACE ( 'NONE', #229, 1.499999999999999556 ) ;
#2458=CARTESIAN_POINT ( 'NONE',  ( 2.168404344971008868E-16, -0.5773502691896253980, 1.000000000000000000 ) ) ;
#2462=ORIENTED_EDGE ( 'NONE', *, *, #184, .T. ) ;
#2463=PLANE ( 'NONE',  #215 ) ;
#2467=CARTESIAN_POINT ( 'NONE',  ( 1.040000000000000036, -0.5773502691896253980, 1.000000000000000000 ) ) ;
#2468=DIRECTION ( 'NONE',  ( -0.000000000000000000, 0.000000000000000000, -1.000000000000000000 ) ) ;
#2470=CARTESIAN_POINT ( 'NONE',  ( 1.040000000000000036, 0.000000000000000000, 0.000000000000000000 ) ) ;
#2471=DIRECTION ( 'NONE',  ( -0.000000000000000000, 0.000000000000000000, 1.000000000000000000 ) ) ;
#2472=ORIENTED_EDGE ( 'NONE', *, *, #3037, .T. ) ;
#2475=ORIENTED_EDGE ( 'NONE', *, *, #1772, .T. ) ;
#2477=EDGE_CURVE ( 'NONE', #1860, #628, #3056, .T. ) ;
#2479=CARTESIAN_POINT ( 'NONE',  ( -998.3826497308103853, 0.000000000000000000, 0.000000000000000000 ) ) ;
#2487=DIRECTION ( 'NONE',  ( -1.000000000000000000, 0.000000000000000000, 0.000000000000000000 ) ) ;
#2489=EDGE_CURVE ( 'NONE', #169, #373, #547, .T. ) ;
#2490=EDGE_LOOP ( 'NONE', ( #2123, #1771, #1856, #1539 ) ) ;
#2491=ORIENTED_EDGE ( 'NONE', *, *, #721, .T. ) ;
#2492=CARTESIAN_POINT ( 'NONE',  ( 1.269999999999999796, 2.849999999999999645, 0.000000000000000000 ) ) ;
#2496=PLANE ( 'NONE',  #701 ) ;
#2497=EDGE_CURVE ( 'NONE', #2346, #1904, #1421, .T. ) ;
#2501=VECTOR ( 'NONE', #935, 1000.000000000000000 ) ;
#2504=ORIENTED_EDGE ( 'NONE', *, *, #337, .F. ) ;
#2505=ORIENTED_EDGE ( 'NONE', *, *, #220, .F. ) ;
#2509=DIRECTION ( 'NONE',  ( -1.000000000000000000, -0.000000000000000000, -0.000000000000000000 ) ) ;
#2517=CONICAL_SURFACE ( 'NONE', #2219, 1.219500000000000028, 0.7853981633974487231 ) ;
#2525=LINE ( 'NONE', #1191, #1698 ) ;
#2528=ADVANCED_FACE ( 'NONE', ( #1183 ), #2517, .T. ) ;
#2533=ORIENTED_EDGE ( 'NONE', *, *, #2489, .F. ) ;
#2535=CARTESIAN_POINT ( 'NONE',  ( 0.000000000000000000, 0.000000000000000000, 0.000000000000000000 ) ) ;
#2538=EDGE_LOOP ( 'NONE', ( #3179, #43 ) ) ;
#2540=DIRECTION ( 'NONE',  ( 0.000000000000000000, 0.000000000000000000, 1.000000000000000000 ) ) ;
#2542=ORIENTED_EDGE ( 'NONE', *, *, #2477, .T. ) ;
#2546=ORIENTED_EDGE ( 'NONE', *, *, #748, .F. ) ;
#2550=VECTOR ( 'NONE', #786, 999.9999999999998863 ) ;
#2555=ORIENTED_EDGE ( 'NONE', *, *, #1701, .T. ) ;
#2562=VECTOR ( 'NONE', #1791, 1000.000000000000227 ) ;
#2563=LINE ( 'NONE', #1154, #1112 ) ;
#2565=VECTOR ( 'NONE', #1035, 1000.000000000000000 ) ;
#2568=ORIENTED_EDGE ( 'NONE', *, *, #1619, .T. ) ;
#2569=LINE ( 'NONE', #350, #1801 ) ;
#2573=DIRECTION ( 'NONE',  ( -0.000000000000000000, 0.5000000000000003331, -0.8660254037844383745 ) ) ;
#2574=DIRECTION ( 'NONE',  ( -0.000000000000000000, -0.5000000000000003331, -0.8660254037844383745 ) ) ;
#2575=ADVANCED_FACE ( 'NONE', ( #1209 ), #2953, .T. ) ;
#2577=EDGE_LOOP ( 'NONE', ( #2601, #305, #2462, #2872, #763 ) ) ;
#2593=EDGE_CURVE ( 'NONE', #1178, #2825, #1197, .T. ) ;
#2594=FACE_OUTER_BOUND ( 'NONE', #2133, .T. ) ;
#2599=CARTESIAN_POINT ( 'NONE',  ( 1.649999999999999911, 0.000000000000000000, 0.000000000000000000 ) ) ;
#2601=ORIENTED_EDGE ( 'NONE', *, *, #1912, .T. ) ;
#2604=CARTESIAN_POINT ( 'NONE',  ( 1.040000000000000036, -1.154700538379251684, -1.199226976249124676E-17 ) ) ;
#2610=CIRCLE ( 'NONE', #110, 1.499999999999999556 ) ;
#2612=MECHANICAL_DESIGN_GEOMETRIC_PRESENTATION_REPRESENTATION('',(#595),#1582);
#2615=AXIS2_PLACEMENT_3D ( 'NONE', #996, #1559, #2034 ) ;
#2619=EDGE_CURVE ( 'NONE', #2676, #401, #1949, .T. ) ;
#2632=FACE_OUTER_BOUND ( 'NONE', #88, .T. ) ;
#2635=DIRECTION ( 'NONE',  ( -0.000000000000000000, 1.000000000000000000, -0.000000000000000000 ) ) ;
#2638=CARTESIAN_POINT ( 'NONE',  ( 1.649999999999999911, 0.000000000000000000, 1.599999999999999645 ) ) ;
#2641=CARTESIAN_POINT ( 'NONE',  ( 1.040000000000000036, 0.5773502691896263972, -1.000000000000000000 ) ) ;
#2646=ORIENTED_EDGE ( 'NONE', *, *, #733, .F. ) ;
#2650=ORIENTED_EDGE ( 'NONE', *, *, #2497, .F. ) ;
#2654=DIRECTION ( 'NONE',  ( -1.000000000000000000, -0.000000000000000000, -0.000000000000000000 ) ) ;
#2662=ADVANCED_FACE ( 'NONE', ( #480 ), #2463, .T. ) ;
#2665=AXIS2_PLACEMENT_3D ( 'NONE', #2171, #719, #2419 ) ;
#2674=AXIS2_PLACEMENT_3D ( 'NONE', #145, #1418, #1945 ) ;
#2676=VERTEX_POINT ( 'NONE', #453 ) ;
#2677=STYLED_ITEM ( 'NONE', ( #343 ), #824 ) ;
#2682=CARTESIAN_POINT ( 'NONE',  ( 7.650000000000000355, 0.000000000000000000, 0.000000000000000000 ) ) ;
#2693=DIRECTION ( 'NONE',  ( -0.000000000000000000, -1.000000000000000000, -0.000000000000000000 ) ) ;
#2696=LINE ( 'NONE', #2467, #2501 ) ;
#2697=DIRECTION ( 'NONE',  ( -1.000000000000000000, -0.000000000000000000, -0.000000000000000000 ) ) ;
#2704=ORIENTED_EDGE ( 'NONE', *, *, #270, .T. ) ;
#2706=CARTESIAN_POINT ( 'NONE',  ( 1.040000000000000036, -0.5773502691896253980, -1.000000000000000000 ) ) ;
#2711=PLANE ( 'NONE',  #1998 ) ;
#2717=DIRECTION ( 'NONE',  ( -0.000000000000000000, 0.000000000000000000, -1.000000000000000000 ) ) ;
#2724=AXIS2_PLACEMENT_3D ( 'NONE', #385, #2808, #1833 ) ;
#2727=DIRECTION ( 'NONE',  ( 0.000000000000000000, 0.8660254037844384856, 0.5000000000000004441 ) ) ;
#2732=ADVANCED_FACE ( 'NONE', ( #483 ), #3072, .T. ) ;
#2738=CARTESIAN_POINT ( 'NONE',  ( 7.650000000000000355, 0.000000000000000000, 0.000000000000000000 ) ) ;
#2761=EDGE_CURVE ( 'NONE', #2825, #1860, #2696, .T. ) ;
#2762=PRODUCT_DEFINITION_CONTEXT ( 'detailed design', #1850, 'design' ) ;
#2764=( NAMED_UNIT ( * ) PLANE_ANGLE_UNIT ( ) SI_UNIT ( $, .RADIAN. ) );
#2766=CARTESIAN_POINT ( 'NONE',  ( 1.040000000000000036, -0.5773502691896253980, 1.000000000000000000 ) ) ;
#2775=AXIS2_PLACEMENT_3D ( 'NONE', #1657, #124, #2122 ) ;
#2779=EDGE_CURVE ( 'NONE', #815, #2850, #1519, .T. ) ;
#2786=EDGE_LOOP ( 'NONE', ( #830, #2341, #1043, #2646, #2999 ) ) ;
#2789=CARTESIAN_POINT ( 'NONE',  ( 1.040000000000000036, -0.5773502691896253980, 1.000000000000000000 ) ) ;
#2792=DIRECTION ( 'NONE',  ( 1.000000000000000000, 0.000000000000000000, -0.000000000000000000 ) ) ;
#2794=( LENGTH_UNIT ( ) NAMED_UNIT ( * ) SI_UNIT ( .MILLI., .METRE. ) );
#2796=AXIS2_PLACEMENT_3D ( 'NONE', #187, #936, #1185 ) ;
#2799=DIRECTION ( 'NONE',  ( 0.000000000000000000, 0.000000000000000000, 1.000000000000000000 ) ) ;
#2800=EDGE_CURVE ( 'NONE', #914, #3197, #950, .T. ) ;
#2802=ADVANCED_FACE ( 'NONE', ( #2275 ), #1014, .T. ) ;
#2804=ORIENTED_EDGE ( 'NONE', *, *, #3093, .F. ) ;
#2808=DIRECTION ( 'NONE',  ( -1.000000000000000000, -0.000000000000000000, -0.000000000000000000 ) ) ;
#2809=LINE ( 'NONE', #648, #460 ) ;
#2810=SURFACE_SIDE_STYLE ('',( #822 ) ) ;
#2813=AXIS2_PLACEMENT_3D ( 'NONE', #3205, #2928, #968 ) ;
#2816=ADVANCED_FACE ( 'NONE', ( #2064 ), #1204, .F. ) ;
#2818=VERTEX_POINT ( 'NONE', #1556 ) ;
#2825=VERTEX_POINT ( 'NONE', #3034 ) ;
#2834=ORIENTED_EDGE ( 'NONE', *, *, #456, .F. ) ;
#2837=CARTESIAN_POINT ( 'NONE',  ( 1.649999999999999911, 0.000000000000000000, 2.849999999999999645 ) ) ;
#2839=VERTEX_POINT ( 'NONE', #1063 ) ;
#2841=CYLINDRICAL_SURFACE ( 'NONE', #1780, 1.499999999999999556 ) ;
#2845=AXIS2_PLACEMENT_3D ( 'NONE', #1126, #400, #2142 ) ;
#2846=LINE ( 'NONE', #3124, #1695 ) ;
#2848=ORIENTED_EDGE ( 'NONE', *, *, #354, .F. ) ;
#2850=VERTEX_POINT ( 'NONE', #1305 ) ;
#2852=EDGE_CURVE ( 'NONE', #1890, #3213, #1240, .T. ) ;
#2853=LINE ( 'NONE', #82, #3104 ) ;
#2858=FACE_BOUND ( 'NONE', #1096, .T. ) ;
#2860=UNCERTAINTY_MEASURE_WITH_UNIT (LENGTH_MEASURE( 1.000000000000000082E-05 ), #2794, 'distance_accuracy_value', 'NONE');
#2864=EDGE_CURVE ( 'NONE', #2348, #2839, #1506, .T. ) ;
#2870=DIRECTION ( 'NONE',  ( 0.000000000000000000, 0.000000000000000000, 1.000000000000000000 ) ) ;
#2871=ORIENTED_EDGE ( 'NONE', *, *, #1329, .T. ) ;
#2872=ORIENTED_EDGE ( 'NONE', *, *, #151, .F. ) ;
#2875=LINE ( 'NONE', #1346, #1213 ) ;
#2878=AXIS2_PLACEMENT_3D ( 'NONE', #3071, #2799, #1837 ) ;
#2880=TOROIDAL_SURFACE ( 'NONE', #1001, 1.599999999999999645, 0.1000000000000000056 ) ;
#2882=VECTOR ( 'NONE', #59, 1000.000000000000000 ) ;
#2884=FACE_OUTER_BOUND ( 'NONE', #2069, .T. ) ;
#2886=ORIENTED_EDGE ( 'NONE', *, *, #2477, .F. ) ;
#2889=ORIENTED_EDGE ( 'NONE', *, *, #2779, .T. ) ;
#2896=ORIENTED_EDGE ( 'NONE', *, *, #456, .T. ) ;
#2899=CIRCLE ( 'NONE', #767, 2.849999999999999645 ) ;
#2900=ADVANCED_FACE ( 'NONE', ( #1522 ), #2305, .T. ) ;
#2902=ORIENTED_EDGE ( 'NONE', *, *, #566, .T. ) ;
#2904=CARTESIAN_POINT ( 'NONE',  ( 4.336808689942017736E-16, 1.424999999999999822, 0.000000000000000000 ) ) ;
#2907=DIRECTION ( 'NONE',  ( -1.000000000000000000, 0.000000000000000000, -0.000000000000000000 ) ) ;
#2911=DIRECTION ( 'NONE',  ( -1.000000000000000000, -0.000000000000000000, -0.000000000000000000 ) ) ;
#2915=DIRECTION ( 'NONE',  ( 1.000000000000000000, 0.000000000000000000, 0.000000000000000000 ) ) ;
#2918=ORIENTED_EDGE ( 'NONE', *, *, #1463, .T. ) ;
#2928=DIRECTION ( 'NONE',  ( -1.000000000000000000, -0.000000000000000000, -0.000000000000000000 ) ) ;
#2929=CARTESIAN_POINT ( 'NONE',  ( 4.336808689942017736E-16, -1.425000000000000044, -2.617682533177466553E-16 ) ) ;
#2931=DIRECTION ( 'NONE',  ( -1.000000000000000000, 0.000000000000000000, 0.000000000000000000 ) ) ;
#2934=VECTOR ( 'NONE', #2487, 1000.000000000000000 ) ;
#2936=CARTESIAN_POINT ( 'NONE',  ( 0.000000000000000000, 0.000000000000000000, 0.000000000000000000 ) ) ;
#2947=CARTESIAN_POINT ( 'NONE',  ( 1.617350269189632428, 0.000000000000000000, 0.000000000000000000 ) ) ;
#2952=ORIENTED_EDGE ( 'NONE', *, *, #2800, .F. ) ;
#2953=PLANE ( 'NONE',  #2347 ) ;
#2955=CARTESIAN_POINT ( 'NONE',  ( 1.040000000000000036, -0.8660254037844384856, -0.5000000000000003331 ) ) ;
#2964=EDGE_CURVE ( 'NONE', #628, #914, #2113, .T. ) ;
#2973=VECTOR ( 'NONE', #2693, 1000.000000000000000 ) ;
#2984=CIRCLE ( 'NONE', #496, 1.499999999999999778 ) ;
#2985=LINE ( 'NONE', #1013, #3196 ) ;
#2986=CARTESIAN_POINT ( 'NONE',  ( 1.040000000000000036, 1.154700538379252350, -1.084202172485497162E-16 ) ) ;
#2988=DIRECTION ( 'NONE',  ( 0.000000000000000000, 0.000000000000000000, 1.000000000000000000 ) ) ;
#2992=ORIENTED_EDGE ( 'NONE', *, *, #2593, .F. ) ;
#2999=ORIENTED_EDGE ( 'NONE', *, *, #184, .F. ) ;
#3005=AXIS2_PLACEMENT_3D ( 'NONE', #1241, #3217, #2468 ) ;
#3014=EDGE_CURVE ( 'NONE', #488, #2839, #1955, .T. ) ;
#3023=ORIENTED_EDGE ( 'NONE', *, *, #660, .T. ) ;
#3034=CARTESIAN_POINT ( 'NONE',  ( 1.040000000000000036, 0.000000000000000000, 1.000000000000000000 ) ) ;
#3037=EDGE_CURVE ( 'NONE', #1178, #2346, #2349, .T. ) ;
#3050=DIRECTION ( 'NONE',  ( -1.000000000000000000, -0.000000000000000000, -0.000000000000000000 ) ) ;
#3056=LINE ( 'NONE', #2604, #844 ) ;
#3064=DIRECTION ( 'NONE',  ( 0.000000000000000000, 0.000000000000000000, 1.000000000000000000 ) ) ;
#3071=CARTESIAN_POINT ( 'NONE',  ( 0.000000000000000000, 0.000000000000000000, 0.000000000000000000 ) ) ;
#3072=CONICAL_SURFACE ( 'NONE', #688, 1.219500000000000028, 0.7853981633974487231 ) ;
#3081=AXIS2_PLACEMENT_3D ( 'NONE', #814, #281, #1583 ) ;
#3082=FACE_OUTER_BOUND ( 'NONE', #3106, .T. ) ;
#3083=ORIENTED_EDGE ( 'NONE', *, *, #1463, .F. ) ;
#3093=EDGE_CURVE ( 'NONE', #1756, #815, #1168, .T. ) ;
#3095=VERTEX_POINT ( 'NONE', #2641 ) ;
#3096=DIRECTION ( 'NONE',  ( -1.000000000000000000, -0.000000000000000000, -0.000000000000000000 ) ) ;
#3101=ORIENTED_EDGE ( 'NONE', *, *, #2440, .T. ) ;
#3103=LINE ( 'NONE', #2121, #439 ) ;
#3104=VECTOR ( 'NONE', #2574, 1000.000000000000114 ) ;
#3106=EDGE_LOOP ( 'NONE', ( #1297, #2918, #2491, #752, #2289 ) ) ;
#3108=DIRECTION ( 'NONE',  ( -0.000000000000000000, 0.000000000000000000, -1.000000000000000000 ) ) ;
#3114=ADVANCED_FACE ( 'NONE', ( #431 ), #2445, .T. ) ;
#3118=CARTESIAN_POINT ( 'NONE',  ( 1.040000000000000036, 0.000000000000000000, 0.000000000000000000 ) ) ;
#3120=CIRCLE ( 'NONE', #1513, 2.849999999999999645 ) ;
#3121=UNCERTAINTY_MEASURE_WITH_UNIT (LENGTH_MEASURE( 1.000000000000000082E-05 ), #1854, 'distance_accuracy_value', 'NONE');
#3124=CARTESIAN_POINT ( 'NONE',  ( 0.000000000000000000, 0.5773502691896263972, -1.000000000000000000 ) ) ;
#3125=ORIENTED_EDGE ( 'NONE', *, *, #1734, .F. ) ;
#3133=SHAPE_DEFINITION_REPRESENTATION ( #8, #524 ) ;
#3135=VECTOR ( 'NONE', #1927, 1000.000000000000114 ) ;
#3136=EDGE_CURVE ( 'NONE', #2825, #1108, #550, .T. ) ;
#3137=CARTESIAN_POINT ( 'NONE',  ( 0.000000000000000000, 1.154700538379252350, -1.084202172485497162E-16 ) ) ;
#3139=CLOSED_SHELL ( 'NONE', ( #2816, #2104, #2528, #3114, #1022, #29, #862, #2230, #1174, #3177, #1960, #2732, #1034, #2232, #2575, #2662, #2802, #176, #100, #2900, #2270, #123, #24, #1845, #1663, #1564, #1345 ) ) ;
#3152=( NAMED_UNIT ( * ) SI_UNIT ( $, .STERADIAN. ) SOLID_ANGLE_UNIT ( ) );
#3154=FACE_OUTER_BOUND ( 'NONE', #1871, .T. ) ;
#3159=CARTESIAN_POINT ( 'NONE',  ( 1.040000000000000036, 0.5773502691896263972, 1.000000000000000000 ) ) ;
#3160=ORIENTED_EDGE ( 'NONE', *, *, #947, .F. ) ;
#3167=DIRECTION ( 'NONE',  ( -1.000000000000000000, -0.000000000000000000, -0.000000000000000000 ) ) ;
#3170=DIRECTION ( 'NONE',  ( -1.000000000000000000, -0.000000000000000000, -0.000000000000000000 ) ) ;
#3172=DIRECTION ( 'NONE',  ( -1.000000000000000000, -0.000000000000000000, -0.000000000000000000 ) ) ;
#3174=VECTOR ( 'NONE', #707, 1000.000000000000227 ) ;
#3177=ADVANCED_FACE ( 'NONE', ( #1159, #1710 ), #679, .F. ) ;
#3179=ORIENTED_EDGE ( 'NONE', *, *, #1797, .F. ) ;
#3180=DIRECTION ( 'NONE',  ( 0.000000000000000000, 0.000000000000000000, 1.000000000000000000 ) ) ;
#3186=CARTESIAN_POINT ( 'NONE',  ( 3.033375984251970081, -8.673617379884035472E-16, 0.000000000000000000 ) ) ;
#3196=VECTOR ( 'NONE', #3215, 1000.000000000000114 ) ;
#3197=VERTEX_POINT ( 'NONE', #562 ) ;
#3200=( GEOMETRIC_REPRESENTATION_CONTEXT ( 3 ) GLOBAL_UNCERTAINTY_ASSIGNED_CONTEXT ( ( #3121 ) ) GLOBAL_UNIT_ASSIGNED_CONTEXT ( ( #1854, #1651, #3152 ) ) REPRESENTATION_CONTEXT ( 'NONE', 'WORKASPACE' ) );
#3201=CARTESIAN_POINT ( 'NONE',  ( 0.000000000000000000, -0.5773502691896253980, 1.000000000000000000 ) ) ;
#3203=DIRECTION ( 'NONE',  ( -1.000000000000000000, 0.000000000000000000, 0.000000000000000000 ) ) ;
#3205=CARTESIAN_POINT ( 'NONE',  ( 1.750000000000000000, 0.000000000000000000, 0.000000000000000000 ) ) ;
#3206=FACE_OUTER_BOUND ( 'NONE', #2538, .T. ) ;
#3210=DIRECTION ( 'NONE',  ( -0.000000000000000000, 1.000000000000000000, -0.000000000000000000 ) ) ;
#3213=VERTEX_POINT ( 'NONE', #2057 ) ;
#3215=DIRECTION ( 'NONE',  ( -0.5000000000000042188, 1.060575238724903710E-16, -0.8660254037844361541 ) ) ;
#3217=DIRECTION ( 'NONE',  ( 1.000000000000000000, 0.000000000000000000, -0.000000000000000000 ) ) ;
#3218=CARTESIAN_POINT ( 'NONE',  ( 1.040000000000000036, -1.154700538379251684, 0.000000000000000000 ) ) ;
#3220=DIRECTION ( 'NONE',  ( -1.000000000000000000, -0.000000000000000000, -0.000000000000000000 ) ) ;
#3258=COLOUR_RGB('Black',0.12,0.14,0.17);
#3259=FILL_AREA_STYLE_COLOUR('',#3258);
#3260=FILL_AREA_STYLE('',(#3259));
#3261=SURFACE_STYLE_FILL_AREA(#3260);
#3262=SURFACE_SIDE_STYLE('',(#3261));
#3263=SURFACE_STYLE_USAGE(.BOTH.,#3262);
#3264=PRESENTATION_STYLE_ASSIGNMENT((#3263));
ENDSEC;
END-ISO-10303-21;
